ISO-10303-21;
HEADER;
/* Generated by software containing ST-Developer
 * from STEP Tools, Inc. (www.steptools.com) 
 */

FILE_DESCRIPTION(
/* description */ ('Turntable on roller ring'),
/* implementation_level */ '2;1');

FILE_NAME(
/* name */ 'Outer race retainer (5).step',
/* time_stamp */ '2026-10-28T03:23:59-07:00',
/* author */ (''),
/* organization */ (''),
/* preprocessor_version */ 'ST-DEVELOPER v20.2',
/* originating_system */ 'Autodesk Translation Framework v15.17.0.0',
/* authorisation */ '');

FILE_SCHEMA (('AUTOMOTIVE_DESIGN { 1 0 10303 214 3 1 1 }'));
ENDSEC;

DATA;
#10=MECHANICAL_DESIGN_GEOMETRIC_PRESENTATION_REPRESENTATION('',(#672),#16281);
#553=SHAPE_REPRESENTATION_RELATIONSHIP('SRR','None',#16576,#608);
#608=ADVANCED_BREP_SHAPE_REPRESENTATION('',(#740),#16270);
#672=STYLED_ITEM('',(#16932),#740);
#740=MANIFOLD_SOLID_BREP('Body1',#8417);
#973=FACE_BOUND('',#2412,.T.);
#974=FACE_BOUND('',#2414,.T.);
#1225=PLANE('',#10010);
#1226=PLANE('',#10011);
#1688=FACE_OUTER_BOUND('',#2409,.T.);
#1689=FACE_OUTER_BOUND('',#2410,.T.);
#1690=FACE_OUTER_BOUND('',#2411,.T.);
#1691=FACE_OUTER_BOUND('',#2413,.T.);
#2409=EDGE_LOOP('',(#7409,#7410,#7411,#7412));
#2410=EDGE_LOOP('',(#7413,#7414,#7415,#7416));
#2411=EDGE_LOOP('',(#7417));
#2412=EDGE_LOOP('',(#7418));
#2413=EDGE_LOOP('',(#7419));
#2414=EDGE_LOOP('',(#7420));
#2952=LINE('',#15476,#3435);
#2953=LINE('',#15482,#3436);
#3435=VECTOR('',#12591,1.1);
#3436=VECTOR('',#12598,1.5);
#3861=CIRCLE('',#10005,1.1);
#3862=CIRCLE('',#10006,1.1);
#3863=CIRCLE('',#10008,1.5);
#3864=CIRCLE('',#10009,1.5);
#4537=VERTEX_POINT('',#15473);
#4538=VERTEX_POINT('',#15475);
#4539=VERTEX_POINT('',#15479);
#4540=VERTEX_POINT('',#15481);
#5515=EDGE_CURVE('',#4537,#4537,#3861,.T.);
#5516=EDGE_CURVE('',#4537,#4538,#2952,.T.);
#5517=EDGE_CURVE('',#4538,#4538,#3862,.T.);
#5518=EDGE_CURVE('',#4539,#4539,#3863,.T.);
#5519=EDGE_CURVE('',#4539,#4540,#2953,.T.);
#5520=EDGE_CURVE('',#4540,#4540,#3864,.T.);
#7409=ORIENTED_EDGE('',*,*,#5515,.F.);
#7410=ORIENTED_EDGE('',*,*,#5516,.T.);
#7411=ORIENTED_EDGE('',*,*,#5517,.T.);
#7412=ORIENTED_EDGE('',*,*,#5516,.F.);
#7413=ORIENTED_EDGE('',*,*,#5518,.F.);
#7414=ORIENTED_EDGE('',*,*,#5519,.T.);
#7415=ORIENTED_EDGE('',*,*,#5520,.T.);
#7416=ORIENTED_EDGE('',*,*,#5519,.F.);
#7417=ORIENTED_EDGE('',*,*,#5518,.T.);
#7418=ORIENTED_EDGE('',*,*,#5515,.T.);
#7419=ORIENTED_EDGE('',*,*,#5520,.F.);
#7420=ORIENTED_EDGE('',*,*,#5517,.F.);
#7833=CYLINDRICAL_SURFACE('',#10004,1.1);
#7834=CYLINDRICAL_SURFACE('',#10007,1.5);
#8291=ADVANCED_FACE('',(#1688),#7833,.F.);
#8292=ADVANCED_FACE('',(#1689),#7834,.T.);
#8293=ADVANCED_FACE('',(#1690,#973),#1225,.T.);
#8294=ADVANCED_FACE('',(#1691,#974),#1226,.F.);
#8417=CLOSED_SHELL('',(#8291,#8292,#8293,#8294));
#10003=AXIS2_PLACEMENT_3D('',#15471,#12585,#12586);
#10004=AXIS2_PLACEMENT_3D('',#15472,#12587,#12588);
#10005=AXIS2_PLACEMENT_3D('',#15474,#12589,#12590);
#10006=AXIS2_PLACEMENT_3D('',#15477,#12592,#12593);
#10007=AXIS2_PLACEMENT_3D('',#15478,#12594,#12595);
#10008=AXIS2_PLACEMENT_3D('',#15480,#12596,#12597);
#10009=AXIS2_PLACEMENT_3D('',#15483,#12599,#12600);
#10010=AXIS2_PLACEMENT_3D('',#15484,#12601,#12602);
#10011=AXIS2_PLACEMENT_3D('',#15485,#12603,#12604);
#12585=DIRECTION('axis',(0.,0.,1.));
#12586=DIRECTION('refdir',(1.,0.,0.));
#12587=DIRECTION('center_axis',(0.,1.,0.));
#12588=DIRECTION('ref_axis',(1.,0.,0.));
#12589=DIRECTION('center_axis',(0.,-1.,0.));
#12590=DIRECTION('ref_axis',(1.,0.,0.));
#12591=DIRECTION('',(0.,-1.,0.));
#12592=DIRECTION('center_axis',(0.,-1.,0.));
#12593=DIRECTION('ref_axis',(1.,0.,0.));
#12594=DIRECTION('center_axis',(0.,1.,0.));
#12595=DIRECTION('ref_axis',(1.,0.,0.));
#12596=DIRECTION('center_axis',(0.,1.,0.));
#12597=DIRECTION('ref_axis',(1.,0.,0.));
#12598=DIRECTION('',(0.,-1.,0.));
#12599=DIRECTION('center_axis',(0.,1.,0.));
#12600=DIRECTION('ref_axis',(1.,0.,0.));
#12601=DIRECTION('center_axis',(0.,1.,0.));
#12602=DIRECTION('ref_axis',(1.,0.,0.));
#12603=DIRECTION('center_axis',(0.,1.,0.));
#12604=DIRECTION('ref_axis',(1.,0.,0.));
#15471=CARTESIAN_POINT('',(0.,0.,0.));
#15472=CARTESIAN_POINT('Origin',(0.,15.45,3.5));
#15473=CARTESIAN_POINT('',(-1.1,15.65,3.5));
#15474=CARTESIAN_POINT('Origin',(0.,15.65,3.5));
#15475=CARTESIAN_POINT('',(-1.1,15.45,3.5));
#15476=CARTESIAN_POINT('',(-1.1,15.45,3.5));
#15477=CARTESIAN_POINT('Origin',(0.,15.45,3.5));
#15478=CARTESIAN_POINT('Origin',(0.,15.45,3.5));
#15479=CARTESIAN_POINT('',(-1.5,15.65,3.5));
#15480=CARTESIAN_POINT('Origin',(0.,15.65,3.5));
#15481=CARTESIAN_POINT('',(-1.5,15.45,3.5));
#15482=CARTESIAN_POINT('',(-1.5,15.45,3.5));
#15483=CARTESIAN_POINT('Origin',(0.,15.45,3.5));
#15484=CARTESIAN_POINT('Origin',(0.,15.65,3.5));
#15485=CARTESIAN_POINT('Origin',(0.,15.45,3.5));
#16201=UNCERTAINTY_MEASURE_WITH_UNIT(LENGTH_MEASURE(0.001),#16282,
'DISTANCE_ACCURACY_VALUE',
'Maximum model space distance between geometric entities at asserted c
onnectivities');
#16212=UNCERTAINTY_MEASURE_WITH_UNIT(LENGTH_MEASURE(0.001),#16282,
'DISTANCE_ACCURACY_VALUE',
'Maximum model space distance between geometric entities at asserted c
onnectivities');
#16270=(
GEOMETRIC_REPRESENTATION_CONTEXT(3)
GLOBAL_UNCERTAINTY_ASSIGNED_CONTEXT((#16201))
GLOBAL_UNIT_ASSIGNED_CONTEXT((#16282,#16284,#16285))
REPRESENTATION_CONTEXT('','3D')
);
#16281=(
GEOMETRIC_REPRESENTATION_CONTEXT(3)
GLOBAL_UNCERTAINTY_ASSIGNED_CONTEXT((#16212))
GLOBAL_UNIT_ASSIGNED_CONTEXT((#16282,#16284,#16285))
REPRESENTATION_CONTEXT('','3D')
);
#16282=(
LENGTH_UNIT()
NAMED_UNIT(*)
SI_UNIT(.CENTI.,.METRE.)
);
#16284=(
NAMED_UNIT(*)
PLANE_ANGLE_UNIT()
SI_UNIT($,.RADIAN.)
);
#16285=(
NAMED_UNIT(*)
SI_UNIT($,.STERADIAN.)
SOLID_ANGLE_UNIT()
);
#16343=SHAPE_DEFINITION_REPRESENTATION(#16477,#16576);
#16477=PRODUCT_DEFINITION_SHAPE('',$,#16645);
#16576=SHAPE_REPRESENTATION('',(#10003),#16270);
#16587=PRODUCT_DEFINITION_CONTEXT('part definition',#16793,'design');
#16645=PRODUCT_DEFINITION('Outer race retainer (5)',
'Outer race retainer (5)',#16713,#16587);
#16713=PRODUCT_DEFINITION_FORMATION('',$,#16852);
#16793=APPLICATION_CONTEXT(
'Core Data for Automotive Mechanical Design Process');
#16794=PRODUCT_CONTEXT('part definition',#16793,'mechanical');
#16852=PRODUCT('Outer race retainer (5)','Outer race retainer (5)',
'Outer race retainer (5)',(#16794));
#16926=COLOUR_RGB('Grey',0.48,0.52,0.57);
#16927=FILL_AREA_STYLE_COLOUR('',#16926);
#16928=FILL_AREA_STYLE('',(#16927));
#16929=SURFACE_STYLE_FILL_AREA(#16928);
#16930=SURFACE_SIDE_STYLE('',(#16929));
#16931=SURFACE_STYLE_USAGE(.BOTH.,#16930);
#16932=PRESENTATION_STYLE_ASSIGNMENT((#16931));
ENDSEC;
END-ISO-10303-21;
